ISO-10303-21;
HEADER;
/* Generated by software containing ST-Developer
 * from STEP Tools, Inc. (www.steptools.com) 
 */

FILE_DESCRIPTION(
/* description */ ('Rotary union on bearing shaft'),
/* implementation_level */ '2;1');

FILE_NAME(
/* name */ 'Cap Screw - M5x20.step',
/* time_stamp */ '2026-10-28T03:24:01-07:00',
/* author */ (''),
/* organization */ (''),
/* preprocessor_version */ 'ST-DEVELOPER v20.2',
/* originating_system */ 'Autodesk Translation Framework v15.17.0.0',
/* authorisation */ '');

FILE_SCHEMA (('AUTOMOTIVE_DESIGN { 1 0 10303 214 3 1 1 }'));
ENDSEC;

DATA;
#10=MECHANICAL_DESIGN_GEOMETRIC_PRESENTATION_REPRESENTATION('',(#347),#9448);
#13=ORIENTED_CLOSED_SHELL('',*,#4905,.F.);
#16=BREP_WITH_VOIDS('Body1',#4904,(#13));
#217=CONICAL_SURFACE('',#5794,0.4,0.785398163397448);
#218=CONICAL_SURFACE('',#5798,0.41,0.785398163397448);
#219=CONICAL_SURFACE('',#5802,0.26,0.463647609000806);
#220=CONICAL_SURFACE('',#5806,0.225,0.785398163397448);
#285=SHAPE_REPRESENTATION_RELATIONSHIP('SRR','None',#9587,#312);
#312=ADVANCED_BREP_SHAPE_REPRESENTATION('',(#16),#9447);
#347=STYLED_ITEM('',(#9785),#16);
#486=FACE_BOUND('',#1348,.T.);
#645=PLANE('',#5792);
#646=PLANE('',#5800);
#647=PLANE('',#5808);
#648=PLANE('',#5809);
#649=PLANE('',#5810);
#650=PLANE('',#5811);
#651=PLANE('',#5812);
#652=PLANE('',#5813);
#653=PLANE('',#5814);
#654=PLANE('',#5815);
#655=PLANE('',#5816);
#938=FACE_OUTER_BOUND('',#1343,.T.);
#939=FACE_OUTER_BOUND('',#1344,.T.);
#940=FACE_OUTER_BOUND('',#1345,.T.);
#941=FACE_OUTER_BOUND('',#1346,.T.);
#942=FACE_OUTER_BOUND('',#1347,.T.);
#943=FACE_OUTER_BOUND('',#1349,.T.);
#944=FACE_OUTER_BOUND('',#1350,.T.);
#945=FACE_OUTER_BOUND('',#1351,.T.);
#946=FACE_OUTER_BOUND('',#1352,.T.);
#947=FACE_OUTER_BOUND('',#1353,.T.);
#948=FACE_OUTER_BOUND('',#1354,.T.);
#949=FACE_OUTER_BOUND('',#1355,.T.);
#950=FACE_OUTER_BOUND('',#1356,.T.);
#951=FACE_OUTER_BOUND('',#1357,.T.);
#952=FACE_OUTER_BOUND('',#1358,.T.);
#953=FACE_OUTER_BOUND('',#1359,.T.);
#954=FACE_OUTER_BOUND('',#1360,.T.);
#1343=EDGE_LOOP('',(#4415));
#1344=EDGE_LOOP('',(#4416,#4417,#4418,#4419));
#1345=EDGE_LOOP('',(#4420,#4421,#4422,#4423));
#1346=EDGE_LOOP('',(#4424,#4425,#4426,#4427));
#1347=EDGE_LOOP('',(#4428));
#1348=EDGE_LOOP('',(#4429));
#1349=EDGE_LOOP('',(#4430,#4431,#4432,#4433));
#1350=EDGE_LOOP('',(#4434,#4435,#4436,#4437));
#1351=EDGE_LOOP('',(#4438,#4439,#4440,#4441));
#1352=EDGE_LOOP('',(#4442));
#1353=EDGE_LOOP('',(#4443,#4444,#4445,#4446));
#1354=EDGE_LOOP('',(#4447,#4448,#4449,#4450));
#1355=EDGE_LOOP('',(#4451,#4452,#4453,#4454));
#1356=EDGE_LOOP('',(#4455,#4456,#4457,#4458));
#1357=EDGE_LOOP('',(#4459,#4460,#4461,#4462));
#1358=EDGE_LOOP('',(#4463,#4464,#4465,#4466));
#1359=EDGE_LOOP('',(#4467,#4468,#4469,#4470,#4471,#4472));
#1360=EDGE_LOOP('',(#4473,#4474,#4475,#4476,#4477,#4478));
#1657=LINE('',#9311,#1977);
#1658=LINE('',#9315,#1978);
#1659=LINE('',#9319,#1979);
#1660=LINE('',#9326,#1980);
#1661=LINE('',#9330,#1981);
#1662=LINE('',#9334,#1982);
#1663=LINE('',#9339,#1983);
#1664=LINE('',#9341,#1984);
#1665=LINE('',#9343,#1985);
#1666=LINE('',#9344,#1986);
#1667=LINE('',#9347,#1987);
#1668=LINE('',#9349,#1988);
#1669=LINE('',#9350,#1989);
#1670=LINE('',#9353,#1990);
#1671=LINE('',#9355,#1991);
#1672=LINE('',#9356,#1992);
#1673=LINE('',#9359,#1993);
#1674=LINE('',#9361,#1994);
#1675=LINE('',#9362,#1995);
#1676=LINE('',#9365,#1996);
#1677=LINE('',#9367,#1997);
#1678=LINE('',#9368,#1998);
#1679=LINE('',#9370,#1999);
#1680=LINE('',#9371,#2000);
#1977=VECTOR('',#7308,0.4);
#1978=VECTOR('',#7313,0.425);
#1979=VECTOR('',#7318,0.41);
#1980=VECTOR('',#7327,0.26);
#1981=VECTOR('',#7332,0.25);
#1982=VECTOR('',#7337,0.225);
#1983=VECTOR('',#7342,1.);
#1984=VECTOR('',#7343,1.);
#1985=VECTOR('',#7344,1.);
#1986=VECTOR('',#7345,1.);
#1987=VECTOR('',#7348,1.);
#1988=VECTOR('',#7349,1.);
#1989=VECTOR('',#7350,1.);
#1990=VECTOR('',#7353,1.);
#1991=VECTOR('',#7354,1.);
#1992=VECTOR('',#7355,1.);
#1993=VECTOR('',#7358,1.);
#1994=VECTOR('',#7359,1.);
#1995=VECTOR('',#7360,1.);
#1996=VECTOR('',#7363,1.);
#1997=VECTOR('',#7364,1.);
#1998=VECTOR('',#7365,1.);
#1999=VECTOR('',#7368,1.);
#2000=VECTOR('',#7369,1.);
#2245=CIRCLE('',#5793,0.375);
#2246=CIRCLE('',#5795,0.425);
#2247=CIRCLE('',#5797,0.425);
#2248=CIRCLE('',#5799,0.395);
#2249=CIRCLE('',#5801,0.27);
#2250=CIRCLE('',#5803,0.24505);
#2251=CIRCLE('',#5805,0.24505);
#2252=CIRCLE('',#5807,0.2);
#2641=VERTEX_POINT('',#9306);
#2642=VERTEX_POINT('',#9309);
#2643=VERTEX_POINT('',#9313);
#2644=VERTEX_POINT('',#9317);
#2645=VERTEX_POINT('',#9321);
#2646=VERTEX_POINT('',#9324);
#2647=VERTEX_POINT('',#9328);
#2648=VERTEX_POINT('',#9332);
#2649=VERTEX_POINT('',#9337);
#2650=VERTEX_POINT('',#9338);
#2651=VERTEX_POINT('',#9340);
#2652=VERTEX_POINT('',#9342);
#2653=VERTEX_POINT('',#9346);
#2654=VERTEX_POINT('',#9348);
#2655=VERTEX_POINT('',#9352);
#2656=VERTEX_POINT('',#9354);
#2657=VERTEX_POINT('',#9358);
#2658=VERTEX_POINT('',#9360);
#2659=VERTEX_POINT('',#9364);
#2660=VERTEX_POINT('',#9366);
#3235=EDGE_CURVE('',#2641,#2641,#2245,.T.);
#3236=EDGE_CURVE('',#2642,#2642,#2246,.T.);
#3237=EDGE_CURVE('',#2642,#2641,#1657,.T.);
#3238=EDGE_CURVE('',#2643,#2643,#2247,.T.);
#3239=EDGE_CURVE('',#2643,#2642,#1658,.T.);
#3240=EDGE_CURVE('',#2644,#2644,#2248,.T.);
#3241=EDGE_CURVE('',#2644,#2643,#1659,.T.);
#3242=EDGE_CURVE('',#2645,#2645,#2249,.T.);
#3243=EDGE_CURVE('',#2646,#2646,#2250,.F.);
#3244=EDGE_CURVE('',#2646,#2645,#1660,.T.);
#3245=EDGE_CURVE('',#2647,#2647,#2251,.F.);
#3246=EDGE_CURVE('',#2647,#2646,#1661,.T.);
#3247=EDGE_CURVE('',#2648,#2648,#2252,.T.);
#3248=EDGE_CURVE('',#2648,#2647,#1662,.T.);
#3249=EDGE_CURVE('',#2649,#2650,#1663,.T.);
#3250=EDGE_CURVE('',#2650,#2651,#1664,.T.);
#3251=EDGE_CURVE('',#2651,#2652,#1665,.T.);
#3252=EDGE_CURVE('',#2649,#2652,#1666,.T.);
#3253=EDGE_CURVE('',#2650,#2653,#1667,.T.);
#3254=EDGE_CURVE('',#2653,#2654,#1668,.T.);
#3255=EDGE_CURVE('',#2654,#2651,#1669,.T.);
#3256=EDGE_CURVE('',#2653,#2655,#1670,.T.);
#3257=EDGE_CURVE('',#2655,#2656,#1671,.T.);
#3258=EDGE_CURVE('',#2656,#2654,#1672,.T.);
#3259=EDGE_CURVE('',#2655,#2657,#1673,.T.);
#3260=EDGE_CURVE('',#2657,#2658,#1674,.T.);
#3261=EDGE_CURVE('',#2658,#2656,#1675,.T.);
#3262=EDGE_CURVE('',#2657,#2659,#1676,.T.);
#3263=EDGE_CURVE('',#2659,#2660,#1677,.T.);
#3264=EDGE_CURVE('',#2660,#2658,#1678,.T.);
#3265=EDGE_CURVE('',#2659,#2649,#1679,.T.);
#3266=EDGE_CURVE('',#2652,#2660,#1680,.T.);
#4415=ORIENTED_EDGE('',*,*,#3235,.F.);
#4416=ORIENTED_EDGE('',*,*,#3236,.F.);
#4417=ORIENTED_EDGE('',*,*,#3237,.T.);
#4418=ORIENTED_EDGE('',*,*,#3235,.T.);
#4419=ORIENTED_EDGE('',*,*,#3237,.F.);
#4420=ORIENTED_EDGE('',*,*,#3238,.F.);
#4421=ORIENTED_EDGE('',*,*,#3239,.T.);
#4422=ORIENTED_EDGE('',*,*,#3236,.T.);
#4423=ORIENTED_EDGE('',*,*,#3239,.F.);
#4424=ORIENTED_EDGE('',*,*,#3240,.F.);
#4425=ORIENTED_EDGE('',*,*,#3241,.T.);
#4426=ORIENTED_EDGE('',*,*,#3238,.T.);
#4427=ORIENTED_EDGE('',*,*,#3241,.F.);
#4428=ORIENTED_EDGE('',*,*,#3240,.T.);
#4429=ORIENTED_EDGE('',*,*,#3242,.F.);
#4430=ORIENTED_EDGE('',*,*,#3243,.F.);
#4431=ORIENTED_EDGE('',*,*,#3244,.T.);
#4432=ORIENTED_EDGE('',*,*,#3242,.T.);
#4433=ORIENTED_EDGE('',*,*,#3244,.F.);
#4434=ORIENTED_EDGE('',*,*,#3245,.F.);
#4435=ORIENTED_EDGE('',*,*,#3246,.T.);
#4436=ORIENTED_EDGE('',*,*,#3243,.T.);
#4437=ORIENTED_EDGE('',*,*,#3246,.F.);
#4438=ORIENTED_EDGE('',*,*,#3247,.F.);
#4439=ORIENTED_EDGE('',*,*,#3248,.T.);
#4440=ORIENTED_EDGE('',*,*,#3245,.T.);
#4441=ORIENTED_EDGE('',*,*,#3248,.F.);
#4442=ORIENTED_EDGE('',*,*,#3247,.T.);
#4443=ORIENTED_EDGE('',*,*,#3249,.T.);
#4444=ORIENTED_EDGE('',*,*,#3250,.T.);
#4445=ORIENTED_EDGE('',*,*,#3251,.T.);
#4446=ORIENTED_EDGE('',*,*,#3252,.F.);
#4447=ORIENTED_EDGE('',*,*,#3253,.T.);
#4448=ORIENTED_EDGE('',*,*,#3254,.T.);
#4449=ORIENTED_EDGE('',*,*,#3255,.T.);
#4450=ORIENTED_EDGE('',*,*,#3250,.F.);
#4451=ORIENTED_EDGE('',*,*,#3256,.T.);
#4452=ORIENTED_EDGE('',*,*,#3257,.T.);
#4453=ORIENTED_EDGE('',*,*,#3258,.T.);
#4454=ORIENTED_EDGE('',*,*,#3254,.F.);
#4455=ORIENTED_EDGE('',*,*,#3259,.T.);
#4456=ORIENTED_EDGE('',*,*,#3260,.T.);
#4457=ORIENTED_EDGE('',*,*,#3261,.T.);
#4458=ORIENTED_EDGE('',*,*,#3257,.F.);
#4459=ORIENTED_EDGE('',*,*,#3262,.T.);
#4460=ORIENTED_EDGE('',*,*,#3263,.T.);
#4461=ORIENTED_EDGE('',*,*,#3264,.T.);
#4462=ORIENTED_EDGE('',*,*,#3260,.F.);
#4463=ORIENTED_EDGE('',*,*,#3265,.T.);
#4464=ORIENTED_EDGE('',*,*,#3252,.T.);
#4465=ORIENTED_EDGE('',*,*,#3266,.T.);
#4466=ORIENTED_EDGE('',*,*,#3263,.F.);
#4467=ORIENTED_EDGE('',*,*,#3265,.F.);
#4468=ORIENTED_EDGE('',*,*,#3262,.F.);
#4469=ORIENTED_EDGE('',*,*,#3259,.F.);
#4470=ORIENTED_EDGE('',*,*,#3256,.F.);
#4471=ORIENTED_EDGE('',*,*,#3253,.F.);
#4472=ORIENTED_EDGE('',*,*,#3249,.F.);
#4473=ORIENTED_EDGE('',*,*,#3266,.F.);
#4474=ORIENTED_EDGE('',*,*,#3251,.F.);
#4475=ORIENTED_EDGE('',*,*,#3255,.F.);
#4476=ORIENTED_EDGE('',*,*,#3258,.F.);
#4477=ORIENTED_EDGE('',*,*,#3261,.F.);
#4478=ORIENTED_EDGE('',*,*,#3264,.F.);
#4567=CYLINDRICAL_SURFACE('',#5796,0.425);
#4568=CYLINDRICAL_SURFACE('',#5804,0.24505);
#4851=ADVANCED_FACE('',(#938),#645,.T.);
#4852=ADVANCED_FACE('',(#939),#217,.T.);
#4853=ADVANCED_FACE('',(#940),#4567,.T.);
#4854=ADVANCED_FACE('',(#941),#218,.T.);
#4855=ADVANCED_FACE('',(#942,#486),#646,.T.);
#4856=ADVANCED_FACE('',(#943),#219,.T.);
#4857=ADVANCED_FACE('',(#944),#4568,.T.);
#4858=ADVANCED_FACE('',(#945),#220,.T.);
#4859=ADVANCED_FACE('',(#946),#647,.T.);
#4860=ADVANCED_FACE('',(#947),#648,.F.);
#4861=ADVANCED_FACE('',(#948),#649,.F.);
#4862=ADVANCED_FACE('',(#949),#650,.F.);
#4863=ADVANCED_FACE('',(#950),#651,.F.);
#4864=ADVANCED_FACE('',(#951),#652,.F.);
#4865=ADVANCED_FACE('',(#952),#653,.F.);
#4866=ADVANCED_FACE('',(#953),#654,.F.);
#4867=ADVANCED_FACE('',(#954),#655,.F.);
#4904=CLOSED_SHELL('',(#4851,#4852,#4853,#4854,#4855,#4856,#4857,#4858,
#4859));
#4905=CLOSED_SHELL('',(#4860,#4861,#4862,#4863,#4864,#4865,#4866,#4867));
#5791=AXIS2_PLACEMENT_3D('',#9304,#7298,#7299);
#5792=AXIS2_PLACEMENT_3D('',#9305,#7300,#7301);
#5793=AXIS2_PLACEMENT_3D('',#9307,#7302,#7303);
#5794=AXIS2_PLACEMENT_3D('',#9308,#7304,#7305);
#5795=AXIS2_PLACEMENT_3D('',#9310,#7306,#7307);
#5796=AXIS2_PLACEMENT_3D('',#9312,#7309,#7310);
#5797=AXIS2_PLACEMENT_3D('',#9314,#7311,#7312);
#5798=AXIS2_PLACEMENT_3D('',#9316,#7314,#7315);
#5799=AXIS2_PLACEMENT_3D('',#9318,#7316,#7317);
#5800=AXIS2_PLACEMENT_3D('',#9320,#7319,#7320);
#5801=AXIS2_PLACEMENT_3D('',#9322,#7321,#7322);
#5802=AXIS2_PLACEMENT_3D('',#9323,#7323,#7324);
#5803=AXIS2_PLACEMENT_3D('',#9325,#7325,#7326);
#5804=AXIS2_PLACEMENT_3D('',#9327,#7328,#7329);
#5805=AXIS2_PLACEMENT_3D('',#9329,#7330,#7331);
#5806=AXIS2_PLACEMENT_3D('',#9331,#7333,#7334);
#5807=AXIS2_PLACEMENT_3D('',#9333,#7335,#7336);
#5808=AXIS2_PLACEMENT_3D('',#9335,#7338,#7339);
#5809=AXIS2_PLACEMENT_3D('',#9336,#7340,#7341);
#5810=AXIS2_PLACEMENT_3D('',#9345,#7346,#7347);
#5811=AXIS2_PLACEMENT_3D('',#9351,#7351,#7352);
#5812=AXIS2_PLACEMENT_3D('',#9357,#7356,#7357);
#5813=AXIS2_PLACEMENT_3D('',#9363,#7361,#7362);
#5814=AXIS2_PLACEMENT_3D('',#9369,#7366,#7367);
#5815=AXIS2_PLACEMENT_3D('',#9372,#7370,#7371);
#5816=AXIS2_PLACEMENT_3D('',#9373,#7372,#7373);
#7298=DIRECTION('axis',(0.,0.,1.));
#7299=DIRECTION('refdir',(1.,0.,0.));
#7300=DIRECTION('center_axis',(0.,1.,0.));
#7301=DIRECTION('ref_axis',(0.,0.,1.));
#7302=DIRECTION('center_axis',(0.,-1.,0.));
#7303=DIRECTION('ref_axis',(1.,0.,0.));
#7304=DIRECTION('center_axis',(0.,-1.,0.));
#7305=DIRECTION('ref_axis',(1.,0.,0.));
#7306=DIRECTION('center_axis',(0.,-1.,0.));
#7307=DIRECTION('ref_axis',(1.,0.,0.));
#7308=DIRECTION('',(0.707106781186548,0.707106781186547,8.65956056235493E-17));
#7309=DIRECTION('center_axis',(0.,-1.,0.));
#7310=DIRECTION('ref_axis',(1.,0.,0.));
#7311=DIRECTION('center_axis',(0.,-1.,0.));
#7312=DIRECTION('ref_axis',(1.,0.,0.));
#7313=DIRECTION('',(0.,1.,0.));
#7314=DIRECTION('center_axis',(0.,1.,0.));
#7315=DIRECTION('ref_axis',(1.,0.,0.));
#7316=DIRECTION('center_axis',(0.,-1.,0.));
#7317=DIRECTION('ref_axis',(1.,0.,0.));
#7318=DIRECTION('',(-0.707106781186547,0.707106781186548,-8.65956056235493E-17));
#7319=DIRECTION('center_axis',(0.,-1.,0.));
#7320=DIRECTION('ref_axis',(0.,0.,-1.));
#7321=DIRECTION('center_axis',(0.,-1.,0.));
#7322=DIRECTION('ref_axis',(1.,0.,0.));
#7323=DIRECTION('center_axis',(0.,1.,0.));
#7324=DIRECTION('ref_axis',(1.,0.,0.));
#7325=DIRECTION('center_axis',(0.,1.,0.));
#7326=DIRECTION('ref_axis',(1.,0.,0.));
#7327=DIRECTION('',(-0.447213595499958,0.894427190999916,-5.47678698264203E-17));
#7328=DIRECTION('center_axis',(0.,-1.,0.));
#7329=DIRECTION('ref_axis',(1.,0.,0.));
#7330=DIRECTION('center_axis',(0.,1.,0.));
#7331=DIRECTION('ref_axis',(1.,0.,0.));
#7332=DIRECTION('',(0.,1.,0.));
#7333=DIRECTION('center_axis',(0.,1.,0.));
#7334=DIRECTION('ref_axis',(1.,0.,0.));
#7335=DIRECTION('center_axis',(0.,-1.,0.));
#7336=DIRECTION('ref_axis',(1.,0.,0.));
#7337=DIRECTION('',(-0.707106781186547,0.707106781186548,-8.65956056235493E-17));
#7338=DIRECTION('center_axis',(0.,-1.,0.));
#7339=DIRECTION('ref_axis',(0.,0.,-1.));
#7340=DIRECTION('center_axis',(0.866025403784439,0.,-0.5));
#7341=DIRECTION('ref_axis',(0.5,0.,0.866025403784439));
#7342=DIRECTION('',(-0.5,0.,-0.866025403784439));
#7343=DIRECTION('',(0.,-1.,0.));
#7344=DIRECTION('',(0.5,0.,0.866025403784439));
#7345=DIRECTION('',(0.,-1.,0.));
#7346=DIRECTION('center_axis',(1.20185167898973E-16,0.,-1.));
#7347=DIRECTION('ref_axis',(1.,0.,1.20185167898973E-16));
#7348=DIRECTION('',(-1.,0.,-1.20185167898973E-16));
#7349=DIRECTION('',(0.,-1.,0.));
#7350=DIRECTION('',(1.,0.,1.20185167898973E-16));
#7351=DIRECTION('center_axis',(-0.866025403784439,0.,-0.5));
#7352=DIRECTION('ref_axis',(0.5,0.,-0.866025403784439));
#7353=DIRECTION('',(-0.5,0.,0.866025403784439));
#7354=DIRECTION('',(0.,-1.,0.));
#7355=DIRECTION('',(0.5,0.,-0.866025403784439));
#7356=DIRECTION('center_axis',(-0.866025403784439,0.,0.5));
#7357=DIRECTION('ref_axis',(-0.5,0.,-0.866025403784439));
#7358=DIRECTION('',(0.5,0.,0.866025403784439));
#7359=DIRECTION('',(0.,-1.,0.));
#7360=DIRECTION('',(-0.5,0.,-0.866025403784439));
#7361=DIRECTION('center_axis',(-2.40370335797945E-16,0.,1.));
#7362=DIRECTION('ref_axis',(-1.,0.,-2.40370335797945E-16));
#7363=DIRECTION('',(1.,0.,2.40370335797945E-16));
#7364=DIRECTION('',(0.,-1.,0.));
#7365=DIRECTION('',(-1.,0.,-2.40370335797945E-16));
#7366=DIRECTION('center_axis',(0.866025403784439,0.,0.5));
#7367=DIRECTION('ref_axis',(-0.5,0.,0.866025403784439));
#7368=DIRECTION('',(0.5,0.,-0.866025403784439));
#7369=DIRECTION('',(-0.5,0.,0.866025403784439));
#7370=DIRECTION('center_axis',(0.,1.,0.));
#7371=DIRECTION('ref_axis',(1.,0.,0.));
#7372=DIRECTION('center_axis',(0.,-1.,0.));
#7373=DIRECTION('ref_axis',(0.,0.,-1.));
#9304=CARTESIAN_POINT('',(0.,0.,0.));
#9305=CARTESIAN_POINT('Origin',(0.375,0.5,0.));
#9306=CARTESIAN_POINT('',(-0.375,0.5,-4.59242549680257E-17));
#9307=CARTESIAN_POINT('Origin',(0.,0.5,0.));
#9308=CARTESIAN_POINT('Origin',(0.,0.475,0.));
#9309=CARTESIAN_POINT('',(-0.425,0.45,-5.20474889637625E-17));
#9310=CARTESIAN_POINT('Origin',(0.,0.45,0.));
#9311=CARTESIAN_POINT('',(-0.4,0.475,-4.89858719658941E-17));
#9312=CARTESIAN_POINT('Origin',(0.,0.24,0.));
#9313=CARTESIAN_POINT('',(-0.425,0.0299999999999998,-5.20474889637625E-17));
#9314=CARTESIAN_POINT('Origin',(0.,0.0299999999999998,0.));
#9315=CARTESIAN_POINT('',(-0.425,0.24,-5.20474889637625E-17));
#9316=CARTESIAN_POINT('Origin',(0.,0.0150000000000001,0.));
#9317=CARTESIAN_POINT('',(-0.395,4.85722573273506E-17,-4.83735485663204E-17));
#9318=CARTESIAN_POINT('Origin',(0.,0.,0.));
#9319=CARTESIAN_POINT('',(-0.41,0.0150000000000001,-5.02105187650415E-17));
#9320=CARTESIAN_POINT('Origin',(0.27,0.,0.));
#9321=CARTESIAN_POINT('',(-0.27,0.,-3.30654635769785E-17));
#9322=CARTESIAN_POINT('Origin',(0.,0.,0.));
#9323=CARTESIAN_POINT('Origin',(0.,-0.02,0.));
#9324=CARTESIAN_POINT('',(-0.24505,-0.0498999999999999,3.00099698131059E-17));
#9325=CARTESIAN_POINT('Origin',(0.,-0.0498999999999999,0.));
#9326=CARTESIAN_POINT('',(-0.26,-0.02,-3.18408167778312E-17));
#9327=CARTESIAN_POINT('Origin',(0.,-0.995,0.));
#9328=CARTESIAN_POINT('',(-0.24505,-1.95495,3.00099698131059E-17));
#9329=CARTESIAN_POINT('Origin',(0.,-1.95495,0.));
#9330=CARTESIAN_POINT('',(-0.24505,-0.995,-3.00099698131059E-17));
#9331=CARTESIAN_POINT('Origin',(0.,-1.975,0.));
#9332=CARTESIAN_POINT('',(-0.2,-2.,-2.44929359829471E-17));
#9333=CARTESIAN_POINT('Origin',(0.,-2.,0.));
#9334=CARTESIAN_POINT('',(-0.225,-1.975,-2.75545529808154E-17));
#9335=CARTESIAN_POINT('Origin',(0.,-2.,0.));
#9336=CARTESIAN_POINT('Origin',(0.115470053837925,-0.5,-0.2));
#9337=CARTESIAN_POINT('',(0.23094010767585,-0.5,0.));
#9338=CARTESIAN_POINT('',(0.115470053837925,-0.5,-0.2));
#9339=CARTESIAN_POINT('',(0.23094010767585,-0.5,0.));
#9340=CARTESIAN_POINT('',(0.115470053837925,-0.8,-0.2));
#9341=CARTESIAN_POINT('',(0.115470053837925,-0.5,-0.2));
#9342=CARTESIAN_POINT('',(0.23094010767585,-0.8,0.));
#9343=CARTESIAN_POINT('',(0.23094010767585,-0.8,0.));
#9344=CARTESIAN_POINT('',(0.23094010767585,-0.5,0.));
#9345=CARTESIAN_POINT('Origin',(-0.115470053837925,-0.5,-0.2));
#9346=CARTESIAN_POINT('',(-0.115470053837925,-0.5,-0.2));
#9347=CARTESIAN_POINT('',(0.115470053837925,-0.5,-0.2));
#9348=CARTESIAN_POINT('',(-0.115470053837925,-0.8,-0.2));
#9349=CARTESIAN_POINT('',(-0.115470053837925,-0.5,-0.2));
#9350=CARTESIAN_POINT('',(0.115470053837925,-0.8,-0.2));
#9351=CARTESIAN_POINT('Origin',(-0.23094010767585,-0.5,-2.77555756156289E-17));
#9352=CARTESIAN_POINT('',(-0.23094010767585,-0.5,-2.82820063659975E-17));
#9353=CARTESIAN_POINT('',(-0.115470053837925,-0.5,-0.2));
#9354=CARTESIAN_POINT('',(-0.23094010767585,-0.8,-2.77555756156289E-17));
#9355=CARTESIAN_POINT('',(-0.23094010767585,-0.5,-2.82820063659975E-17));
#9356=CARTESIAN_POINT('',(-0.115470053837925,-0.8,-0.2));
#9357=CARTESIAN_POINT('Origin',(-0.115470053837925,-0.5,0.2));
#9358=CARTESIAN_POINT('',(-0.115470053837925,-0.5,0.2));
#9359=CARTESIAN_POINT('',(-0.23094010767585,-0.5,-2.82820063659975E-17));
#9360=CARTESIAN_POINT('',(-0.115470053837925,-0.8,0.2));
#9361=CARTESIAN_POINT('',(-0.115470053837925,-0.5,0.2));
#9362=CARTESIAN_POINT('',(-0.23094010767585,-0.8,-2.82820063659975E-17));
#9363=CARTESIAN_POINT('Origin',(0.115470053837925,-0.5,0.2));
#9364=CARTESIAN_POINT('',(0.115470053837925,-0.5,0.2));
#9365=CARTESIAN_POINT('',(-0.115470053837925,-0.5,0.2));
#9366=CARTESIAN_POINT('',(0.115470053837925,-0.8,0.2));
#9367=CARTESIAN_POINT('',(0.115470053837925,-0.5,0.2));
#9368=CARTESIAN_POINT('',(-0.115470053837925,-0.8,0.2));
#9369=CARTESIAN_POINT('Origin',(0.23094010767585,-0.5,0.));
#9370=CARTESIAN_POINT('',(0.115470053837925,-0.5,0.2));
#9371=CARTESIAN_POINT('',(0.115470053837925,-0.8,0.2));
#9372=CARTESIAN_POINT('Origin',(0.,-0.5,0.));
#9373=CARTESIAN_POINT('Origin',(0.,-0.8,0.));
#9415=UNCERTAINTY_MEASURE_WITH_UNIT(LENGTH_MEASURE(0.001),#9449,
'DISTANCE_ACCURACY_VALUE',
'Maximum model space distance between geometric entities at asserted c
onnectivities');
#9416=UNCERTAINTY_MEASURE_WITH_UNIT(LENGTH_MEASURE(0.001),#9449,
'DISTANCE_ACCURACY_VALUE',
'Maximum model space distance between geometric entities at asserted c
onnectivities');
#9447=(
GEOMETRIC_REPRESENTATION_CONTEXT(3)
GLOBAL_UNCERTAINTY_ASSIGNED_CONTEXT((#9415))
GLOBAL_UNIT_ASSIGNED_CONTEXT((#9449,#9451,#9452))
REPRESENTATION_CONTEXT('','3D')
);
#9448=(
GEOMETRIC_REPRESENTATION_CONTEXT(3)
GLOBAL_UNCERTAINTY_ASSIGNED_CONTEXT((#9416))
GLOBAL_UNIT_ASSIGNED_CONTEXT((#9449,#9451,#9452))
REPRESENTATION_CONTEXT('','3D')
);
#9449=(
LENGTH_UNIT()
NAMED_UNIT(*)
SI_UNIT(.CENTI.,.METRE.)
);
#9451=(
NAMED_UNIT(*)
PLANE_ANGLE_UNIT()
SI_UNIT($,.RADIAN.)
);
#9452=(
NAMED_UNIT(*)
SI_UNIT($,.STERADIAN.)
SOLID_ANGLE_UNIT()
);
#9483=SHAPE_DEFINITION_REPRESENTATION(#9545,#9587);
#9545=PRODUCT_DEFINITION_SHAPE('',$,#9619);
#9587=SHAPE_REPRESENTATION('',(#5791),#9447);
#9588=PRODUCT_DEFINITION_CONTEXT('part definition',#9683,'design');
#9619=PRODUCT_DEFINITION('Cap Screw - M5x20','Cap Screw - M5x20',#9650,
#9588);
#9650=PRODUCT_DEFINITION_FORMATION('',$,#9715);
#9683=APPLICATION_CONTEXT(
'Core Data for Automotive Mechanical Design Process');
#9684=PRODUCT_CONTEXT('part definition',#9683,'mechanical');
#9715=PRODUCT('Cap Screw - M5x20','Cap Screw - M5x20',
'Cap Screw - M5x20',(#9684));
#9779=COLOUR_RGB('Black',0.12,0.14,0.17);
#9780=FILL_AREA_STYLE_COLOUR('',#9779);
#9781=FILL_AREA_STYLE('',(#9780));
#9782=SURFACE_STYLE_FILL_AREA(#9781);
#9783=SURFACE_SIDE_STYLE('',(#9782));
#9784=SURFACE_STYLE_USAGE(.BOTH.,#9783);
#9785=PRESENTATION_STYLE_ASSIGNMENT((#9784));
ENDSEC;
END-ISO-10303-21;
